ISO-10303-21;
HEADER;
FILE_DESCRIPTION (('STEP AP214'),
    '1' );
FILE_NAME ('sphere.step',
    '2026-10-05T20:10:51',
    ( '' ),
    ( '' ),
    'SwSTEP 2.0',
    'SolidWorks 2020',
    '' );
FILE_SCHEMA (( 'AUTOMOTIVE_DESIGN' ));
ENDSEC;

DATA;
#626=UNCERTAINTY_MEASURE_WITH_UNIT (LENGTH_MEASURE( 1.000000000000000082E-05 ), #100266, 'distance_accuracy_value', 'NONE');
#670=COLOUR_RGB ( '', 0.31764706, 0.68627451, 0.89019608) ;
#1670=( NAMED_UNIT ( * ) SI_UNIT ( $, .STERADIAN. ) SOLID_ANGLE_UNIT ( ) );
#2121=DIRECTION ( 'NONE',  ( 1.000000000000000000, 6.532318089225149424E-16, -4.440892098500620245E-16 ) ) ;
#2734=SURFACE_STYLE_USAGE ( .BOTH. , #182568 ) ;
#3791=SHAPE_REPRESENTATION_RELATIONSHIP ( 'NONE' , 'NONE' ,  #211717, #174158 ) ;
#4839=AXIS2_PLACEMENT_3D ( 'NONE', #21646, #153830, #53117 ) ;
#6365=( NAMED_UNIT ( * ) SI_UNIT ( $, .STERADIAN. ) SOLID_ANGLE_UNIT ( ) );
#11751=APPLICATION_CONTEXT ( 'automotive_design' ) ;
#18174=VERTEX_POINT ( 'NONE', #199348 ) ;
#19009=SHAPE_DEFINITION_REPRESENTATION ( #47232, #211717 ) ;
#20061=( LENGTH_UNIT ( ) NAMED_UNIT ( * ) SI_UNIT ( .MILLI., .METRE. ) );
#21434=ORIENTED_EDGE ( 'NONE', *, *, #125500, .F. ) ;
#21646=CARTESIAN_POINT ( 'NONE',  ( 0.000000000000000000, 0.02011834319527033843, -6.938893903907228378E-15 ) ) ;
#26340=MANIFOLD_SOLID_BREP ( 'Revolve1', #105368 ) ;
#27579=( GEOMETRIC_REPRESENTATION_CONTEXT ( 3 ) GLOBAL_UNCERTAINTY_ASSIGNED_CONTEXT ( ( #626 ) ) GLOBAL_UNIT_ASSIGNED_CONTEXT ( ( #100266, #134926, #1670 ) ) REPRESENTATION_CONTEXT ( 'NONE', 'WORKASPACE' ) );
#28251=VERTEX_POINT ( 'NONE', #35154 ) ;
#29079=ADVANCED_FACE ( 'NONE', ( #164666 ), #84469, .T. ) ;
#29303=FILL_AREA_STYLE_COLOUR ( '', #670 ) ;
#31953=STYLED_ITEM ( 'NONE', ( #211229 ), #26340 ) ;
#34528=( GEOMETRIC_REPRESENTATION_CONTEXT ( 3 ) GLOBAL_UNCERTAINTY_ASSIGNED_CONTEXT ( ( #105395 ) ) GLOBAL_UNIT_ASSIGNED_CONTEXT ( ( #20061, #181509, #82943 ) ) REPRESENTATION_CONTEXT ( 'NONE', 'WORKASPACE' ) );
#35154=CARTESIAN_POINT ( 'NONE',  ( -5.653072611647089601E-16, -1.229881656804728163, -7.771561172376095783E-15 ) ) ;
#42353=FACE_OUTER_BOUND ( 'NONE', #107157, .T. ) ;
#47232=PRODUCT_DEFINITION_SHAPE ( 'NONE', 'NONE',  #151058 ) ;
#47300=UNCERTAINTY_MEASURE_WITH_UNIT (LENGTH_MEASURE( 1.000000000000000082E-05 ), #129018, 'distance_accuracy_value', 'NONE');
#48320=MECHANICAL_DESIGN_GEOMETRIC_PRESENTATION_REPRESENTATION('',(#58663),#34528);
#53117=DIRECTION ( 'NONE',  ( 0.000000000000000000, 1.000000000000000000, 6.661338147750951075E-16 ) ) ;
#57517=SPHERICAL_SURFACE ( 'NONE', #120336, 1.250000000000000000 ) ;
#58663=STYLED_ITEM ( 'NONE', ( #168463 ), #174158 ) ;
#73759=DIRECTION ( 'NONE',  ( 1.000000000000000000, 6.532318089225149424E-16, -4.440892098500620245E-16 ) ) ;
#82943=( NAMED_UNIT ( * ) SI_UNIT ( $, .STERADIAN. ) SOLID_ANGLE_UNIT ( ) );
#84469=SPHERICAL_SURFACE ( 'NONE', #204925, 1.250000000000000000 ) ;
#85079=FILL_AREA_STYLE ('',( #117652 ) ) ;
#88723=( NAMED_UNIT ( * ) PLANE_ANGLE_UNIT ( ) SI_UNIT ( $, .RADIAN. ) );
#91353=CIRCLE ( 'NONE', #4839, 1.250000000000000000 ) ;
#95216=CARTESIAN_POINT ( 'NONE',  ( 0.000000000000000000, 0.000000000000000000, 0.000000000000000000 ) ) ;
#97555=DIRECTION ( 'NONE',  ( -4.440892098500624683E-16, 6.661338147750949103E-16, -1.000000000000000000 ) ) ;
#99867=DIRECTION ( 'NONE',  ( 4.440892098500621231E-16, -6.661338147750950089E-16, 1.000000000000000000 ) ) ;
#100266=( LENGTH_UNIT ( ) NAMED_UNIT ( * ) SI_UNIT ( .MILLI., .METRE. ) );
#100721=CARTESIAN_POINT ( 'NONE',  ( 0.000000000000000000, 0.02011834319527033843, -6.938893903907228378E-15 ) ) ;
#104464=MECHANICAL_DESIGN_GEOMETRIC_PRESENTATION_REPRESENTATION('',(#31953),#118433);
#105368=CLOSED_SHELL ( 'NONE', ( #29079, #151949 ) ) ;
#105395=UNCERTAINTY_MEASURE_WITH_UNIT (LENGTH_MEASURE( 1.000000000000000082E-05 ), #20061, 'distance_accuracy_value', 'NONE');
#107157=EDGE_LOOP ( 'NONE', ( #195706, #151817 ) ) ;
#111662=DIRECTION ( 'NONE',  ( -4.440892098500624683E-16, 6.661338147750949103E-16, -1.000000000000000000 ) ) ;
#115682=EDGE_CURVE ( 'NONE', #28251, #18174, #91353, .T. ) ;
#116574=SURFACE_STYLE_FILL_AREA ( #85079 ) ;
#117620=COLOUR_RGB ( '', 0.31764706, 0.68627451, 0.89019608) ;
#117652=FILL_AREA_STYLE_COLOUR ( '', #117620 ) ;
#118433=( GEOMETRIC_REPRESENTATION_CONTEXT ( 3 ) GLOBAL_UNCERTAINTY_ASSIGNED_CONTEXT ( ( #47300 ) ) GLOBAL_UNIT_ASSIGNED_CONTEXT ( ( #129018, #88723, #6365 ) ) REPRESENTATION_CONTEXT ( 'NONE', 'WORKASPACE' ) );
#120336=AXIS2_PLACEMENT_3D ( 'NONE', #174488, #111662, #73759 ) ;
#125500=EDGE_CURVE ( 'NONE', #28251, #18174, #185457, .T. ) ;
#129018=( LENGTH_UNIT ( ) NAMED_UNIT ( * ) SI_UNIT ( .MILLI., .METRE. ) );
#131830=PRODUCT_DEFINITION_FORMATION_WITH_SPECIFIED_SOURCE ( 'ANY', '', #192368, .NOT_KNOWN. ) ;
#132002=DIRECTION ( 'NONE',  ( 0.000000000000000000, 0.000000000000000000, 1.000000000000000000 ) ) ;
#132405=CARTESIAN_POINT ( 'NONE',  ( 0.000000000000000000, 0.02011834319527033843, -6.938893903907228378E-15 ) ) ;
#132740=PRODUCT_DEFINITION_CONTEXT ( 'detailed design', #195850, 'design' ) ;
#133223=FILL_AREA_STYLE ('',( #29303 ) ) ;
#134926=( NAMED_UNIT ( * ) PLANE_ANGLE_UNIT ( ) SI_UNIT ( $, .RADIAN. ) );
#138302=EDGE_LOOP ( 'NONE', ( #21434, #152130 ) ) ;
#145224=SURFACE_STYLE_USAGE ( .BOTH. , #161449 ) ;
#151058=PRODUCT_DEFINITION ( 'UNKNOWN', '', #131830, #132740 ) ;
#151817=ORIENTED_EDGE ( 'NONE', *, *, #125500, .T. ) ;
#151949=ADVANCED_FACE ( 'NONE', ( #42353 ), #57517, .T. ) ;
#152130=ORIENTED_EDGE ( 'NONE', *, *, #115682, .T. ) ;
#153830=DIRECTION ( 'NONE',  ( -3.216245299353269257E-16, 6.661338147750950089E-16, -1.000000000000000000 ) ) ;
#161266=DIRECTION ( 'NONE',  ( 1.000000000000000000, 0.000000000000000000, 0.000000000000000000 ) ) ;
#161449=SURFACE_SIDE_STYLE ('',( #199229 ) ) ;
#164666=FACE_OUTER_BOUND ( 'NONE', #138302, .T. ) ;
#167005=DIRECTION ( 'NONE',  ( 0.000000000000000000, -1.000000000000000000, -6.661338147750945159E-16 ) ) ;
#168463=PRESENTATION_STYLE_ASSIGNMENT (( #2734 ) ) ;
#174158=ADVANCED_BREP_SHAPE_REPRESENTATION ( '', ( #26340, #200407 ), #27579 ) ;
#174488=CARTESIAN_POINT ( 'NONE',  ( 0.000000000000000000, 0.02011834319527033843, -6.938893903907228378E-15 ) ) ;
#178678=AXIS2_PLACEMENT_3D ( 'NONE', #132405, #99867, #167005 ) ;
#181509=( NAMED_UNIT ( * ) PLANE_ANGLE_UNIT ( ) SI_UNIT ( $, .RADIAN. ) );
#182568=SURFACE_SIDE_STYLE ('',( #116574 ) ) ;
#185457=CIRCLE ( 'NONE', #178678, 1.250000000000000000 ) ;
#192368=PRODUCT ( 'sphere', 'sphere', '', ( #202001 ) ) ;
#195706=ORIENTED_EDGE ( 'NONE', *, *, #115682, .F. ) ;
#195850=APPLICATION_CONTEXT ( 'automotive_design' ) ;
#199229=SURFACE_STYLE_FILL_AREA ( #133223 ) ;
#199348=CARTESIAN_POINT ( 'NONE',  ( 7.183881110581282897E-16, 1.270118343195268951, -6.106226635438360972E-15 ) ) ;
#200407=AXIS2_PLACEMENT_3D ( 'NONE', #95216, #132002, #161266 ) ;
#202001=PRODUCT_CONTEXT ( 'NONE', #11751, 'mechanical' ) ;
#204925=AXIS2_PLACEMENT_3D ( 'NONE', #100721, #97555, #2121 ) ;
#211229=PRESENTATION_STYLE_ASSIGNMENT (( #145224 ) ) ;
#211717=SHAPE_REPRESENTATION ( 'sphere', ( #200407 ), #27579 ) ;
ENDSEC;
END-ISO-10303-21;
